ISO-10303-21;
HEADER;
/* Generated by software containing ST-Developer
 * from STEP Tools, Inc. (www.steptools.com) 
 */

FILE_DESCRIPTION(
/* description */ ('Jaw-coupled motor to shaft test stand'),
/* implementation_level */ '2;1');

FILE_NAME(
/* name */ 'Socket Set Screw - M5x8.step',
/* time_stamp */ '2026-10-27T10:46:06-07:00',
/* author */ (''),
/* organization */ (''),
/* preprocessor_version */ 'ST-DEVELOPER v20.2',
/* originating_system */ 'Autodesk Translation Framework v15.17.0.0',
/* authorisation */ '');

FILE_SCHEMA (('AUTOMOTIVE_DESIGN { 1 0 10303 214 3 1 1 }'));
ENDSEC;

DATA;
#10=MECHANICAL_DESIGN_GEOMETRIC_PRESENTATION_REPRESENTATION('',(#371),#19361);
#23=CONICAL_SURFACE('',#12289,0.235,0.785398163397448);
#24=CONICAL_SURFACE('',#12293,0.2125,0.785398163397448);
#306=SHAPE_REPRESENTATION_RELATIONSHIP('SRR','None',#19523,#338);
#338=ADVANCED_BREP_SHAPE_REPRESENTATION('',(#402),#19359);
#371=STYLED_ITEM('',(#19753),#402);
#402=MANIFOLD_SOLID_BREP('Body1',#11017);
#514=FACE_BOUND('',#2352,.T.);
#1002=PLANE('',#12280);
#1003=PLANE('',#12281);
#1004=PLANE('',#12282);
#1005=PLANE('',#12283);
#1006=PLANE('',#12284);
#1007=PLANE('',#12285);
#1008=PLANE('',#12286);
#1009=PLANE('',#12287);
#1010=PLANE('',#12295);
#1613=FACE_OUTER_BOUND('',#2344,.T.);
#1614=FACE_OUTER_BOUND('',#2345,.T.);
#1615=FACE_OUTER_BOUND('',#2346,.T.);
#1616=FACE_OUTER_BOUND('',#2347,.T.);
#1617=FACE_OUTER_BOUND('',#2348,.T.);
#1618=FACE_OUTER_BOUND('',#2349,.T.);
#1619=FACE_OUTER_BOUND('',#2350,.T.);
#1620=FACE_OUTER_BOUND('',#2351,.T.);
#1621=FACE_OUTER_BOUND('',#2353,.T.);
#1622=FACE_OUTER_BOUND('',#2354,.T.);
#1623=FACE_OUTER_BOUND('',#2355,.T.);
#1624=FACE_OUTER_BOUND('',#2356,.T.);
#2344=EDGE_LOOP('',(#10156,#10157,#10158,#10159));
#2345=EDGE_LOOP('',(#10160,#10161,#10162,#10163));
#2346=EDGE_LOOP('',(#10164,#10165,#10166,#10167));
#2347=EDGE_LOOP('',(#10168,#10169,#10170,#10171));
#2348=EDGE_LOOP('',(#10172,#10173,#10174,#10175));
#2349=EDGE_LOOP('',(#10176,#10177,#10178,#10179));
#2350=EDGE_LOOP('',(#10180,#10181,#10182,#10183,#10184,#10185));
#2351=EDGE_LOOP('',(#10186));
#2352=EDGE_LOOP('',(#10187,#10188,#10189,#10190,#10191,#10192));
#2353=EDGE_LOOP('',(#10193,#10194,#10195,#10196));
#2354=EDGE_LOOP('',(#10197,#10198,#10199,#10200));
#2355=EDGE_LOOP('',(#10201,#10202,#10203,#10204));
#2356=EDGE_LOOP('',(#10205));
#3483=LINE('',#19148,#4636);
#3484=LINE('',#19150,#4637);
#3485=LINE('',#19152,#4638);
#3486=LINE('',#19153,#4639);
#3487=LINE('',#19156,#4640);
#3488=LINE('',#19158,#4641);
#3489=LINE('',#19159,#4642);
#3490=LINE('',#19162,#4643);
#3491=LINE('',#19164,#4644);
#3492=LINE('',#19165,#4645);
#3493=LINE('',#19168,#4646);
#3494=LINE('',#19170,#4647);
#3495=LINE('',#19171,#4648);
#3496=LINE('',#19174,#4649);
#3497=LINE('',#19176,#4650);
#3498=LINE('',#19177,#4651);
#3499=LINE('',#19179,#4652);
#3500=LINE('',#19180,#4653);
#3501=LINE('',#19188,#4654);
#3502=LINE('',#19192,#4655);
#3503=LINE('',#19196,#4656);
#4636=VECTOR('',#15264,1.);
#4637=VECTOR('',#15265,1.);
#4638=VECTOR('',#15266,1.);
#4639=VECTOR('',#15267,1.);
#4640=VECTOR('',#15270,1.);
#4641=VECTOR('',#15271,1.);
#4642=VECTOR('',#15272,1.);
#4643=VECTOR('',#15275,1.);
#4644=VECTOR('',#15276,1.);
#4645=VECTOR('',#15277,1.);
#4646=VECTOR('',#15280,1.);
#4647=VECTOR('',#15281,1.);
#4648=VECTOR('',#15282,1.);
#4649=VECTOR('',#15285,1.);
#4650=VECTOR('',#15286,1.);
#4651=VECTOR('',#15287,1.);
#4652=VECTOR('',#15290,1.);
#4653=VECTOR('',#15291,1.);
#4654=VECTOR('',#15302,0.235);
#4655=VECTOR('',#15307,0.25);
#4656=VECTOR('',#15312,0.2125);
#4931=CIRCLE('',#12288,0.22);
#4932=CIRCLE('',#12290,0.24505);
#4933=CIRCLE('',#12292,0.24505);
#4934=CIRCLE('',#12294,0.175);
#5848=VERTEX_POINT('',#19146);
#5849=VERTEX_POINT('',#19147);
#5850=VERTEX_POINT('',#19149);
#5851=VERTEX_POINT('',#19151);
#5852=VERTEX_POINT('',#19155);
#5853=VERTEX_POINT('',#19157);
#5854=VERTEX_POINT('',#19161);
#5855=VERTEX_POINT('',#19163);
#5856=VERTEX_POINT('',#19167);
#5857=VERTEX_POINT('',#19169);
#5858=VERTEX_POINT('',#19173);
#5859=VERTEX_POINT('',#19175);
#5860=VERTEX_POINT('',#19183);
#5861=VERTEX_POINT('',#19186);
#5862=VERTEX_POINT('',#19190);
#5863=VERTEX_POINT('',#19194);
#7289=EDGE_CURVE('',#5848,#5849,#3483,.T.);
#7290=EDGE_CURVE('',#5848,#5850,#3484,.T.);
#7291=EDGE_CURVE('',#5850,#5851,#3485,.T.);
#7292=EDGE_CURVE('',#5849,#5851,#3486,.T.);
#7293=EDGE_CURVE('',#5852,#5848,#3487,.T.);
#7294=EDGE_CURVE('',#5852,#5853,#3488,.T.);
#7295=EDGE_CURVE('',#5853,#5850,#3489,.T.);
#7296=EDGE_CURVE('',#5854,#5852,#3490,.T.);
#7297=EDGE_CURVE('',#5854,#5855,#3491,.T.);
#7298=EDGE_CURVE('',#5855,#5853,#3492,.T.);
#7299=EDGE_CURVE('',#5856,#5854,#3493,.T.);
#7300=EDGE_CURVE('',#5856,#5857,#3494,.T.);
#7301=EDGE_CURVE('',#5857,#5855,#3495,.T.);
#7302=EDGE_CURVE('',#5858,#5856,#3496,.T.);
#7303=EDGE_CURVE('',#5858,#5859,#3497,.T.);
#7304=EDGE_CURVE('',#5859,#5857,#3498,.T.);
#7305=EDGE_CURVE('',#5849,#5858,#3499,.T.);
#7306=EDGE_CURVE('',#5851,#5859,#3500,.T.);
#7307=EDGE_CURVE('',#5860,#5860,#4931,.T.);
#7308=EDGE_CURVE('',#5861,#5861,#4932,.T.);
#7309=EDGE_CURVE('',#5861,#5860,#3501,.T.);
#7310=EDGE_CURVE('',#5862,#5862,#4933,.F.);
#7311=EDGE_CURVE('',#5862,#5861,#3502,.T.);
#7312=EDGE_CURVE('',#5863,#5863,#4934,.T.);
#7313=EDGE_CURVE('',#5863,#5862,#3503,.T.);
#10156=ORIENTED_EDGE('',*,*,#7289,.F.);
#10157=ORIENTED_EDGE('',*,*,#7290,.T.);
#10158=ORIENTED_EDGE('',*,*,#7291,.T.);
#10159=ORIENTED_EDGE('',*,*,#7292,.F.);
#10160=ORIENTED_EDGE('',*,*,#7293,.F.);
#10161=ORIENTED_EDGE('',*,*,#7294,.T.);
#10162=ORIENTED_EDGE('',*,*,#7295,.T.);
#10163=ORIENTED_EDGE('',*,*,#7290,.F.);
#10164=ORIENTED_EDGE('',*,*,#7296,.F.);
#10165=ORIENTED_EDGE('',*,*,#7297,.T.);
#10166=ORIENTED_EDGE('',*,*,#7298,.T.);
#10167=ORIENTED_EDGE('',*,*,#7294,.F.);
#10168=ORIENTED_EDGE('',*,*,#7299,.F.);
#10169=ORIENTED_EDGE('',*,*,#7300,.T.);
#10170=ORIENTED_EDGE('',*,*,#7301,.T.);
#10171=ORIENTED_EDGE('',*,*,#7297,.F.);
#10172=ORIENTED_EDGE('',*,*,#7302,.F.);
#10173=ORIENTED_EDGE('',*,*,#7303,.T.);
#10174=ORIENTED_EDGE('',*,*,#7304,.T.);
#10175=ORIENTED_EDGE('',*,*,#7300,.F.);
#10176=ORIENTED_EDGE('',*,*,#7305,.F.);
#10177=ORIENTED_EDGE('',*,*,#7292,.T.);
#10178=ORIENTED_EDGE('',*,*,#7306,.T.);
#10179=ORIENTED_EDGE('',*,*,#7303,.F.);
#10180=ORIENTED_EDGE('',*,*,#7306,.F.);
#10181=ORIENTED_EDGE('',*,*,#7291,.F.);
#10182=ORIENTED_EDGE('',*,*,#7295,.F.);
#10183=ORIENTED_EDGE('',*,*,#7298,.F.);
#10184=ORIENTED_EDGE('',*,*,#7301,.F.);
#10185=ORIENTED_EDGE('',*,*,#7304,.F.);
#10186=ORIENTED_EDGE('',*,*,#7307,.F.);
#10187=ORIENTED_EDGE('',*,*,#7289,.T.);
#10188=ORIENTED_EDGE('',*,*,#7305,.T.);
#10189=ORIENTED_EDGE('',*,*,#7302,.T.);
#10190=ORIENTED_EDGE('',*,*,#7299,.T.);
#10191=ORIENTED_EDGE('',*,*,#7296,.T.);
#10192=ORIENTED_EDGE('',*,*,#7293,.T.);
#10193=ORIENTED_EDGE('',*,*,#7308,.F.);
#10194=ORIENTED_EDGE('',*,*,#7309,.T.);
#10195=ORIENTED_EDGE('',*,*,#7307,.T.);
#10196=ORIENTED_EDGE('',*,*,#7309,.F.);
#10197=ORIENTED_EDGE('',*,*,#7310,.F.);
#10198=ORIENTED_EDGE('',*,*,#7311,.T.);
#10199=ORIENTED_EDGE('',*,*,#7308,.T.);
#10200=ORIENTED_EDGE('',*,*,#7311,.F.);
#10201=ORIENTED_EDGE('',*,*,#7312,.F.);
#10202=ORIENTED_EDGE('',*,*,#7313,.T.);
#10203=ORIENTED_EDGE('',*,*,#7310,.T.);
#10204=ORIENTED_EDGE('',*,*,#7313,.F.);
#10205=ORIENTED_EDGE('',*,*,#7312,.T.);
#10361=CYLINDRICAL_SURFACE('',#12291,0.24505);
#10955=ADVANCED_FACE('',(#1613),#1002,.F.);
#10956=ADVANCED_FACE('',(#1614),#1003,.F.);
#10957=ADVANCED_FACE('',(#1615),#1004,.F.);
#10958=ADVANCED_FACE('',(#1616),#1005,.F.);
#10959=ADVANCED_FACE('',(#1617),#1006,.F.);
#10960=ADVANCED_FACE('',(#1618),#1007,.F.);
#10961=ADVANCED_FACE('',(#1619),#1008,.F.);
#10962=ADVANCED_FACE('',(#1620,#514),#1009,.T.);
#10963=ADVANCED_FACE('',(#1621),#23,.T.);
#10964=ADVANCED_FACE('',(#1622),#10361,.T.);
#10965=ADVANCED_FACE('',(#1623),#24,.T.);
#10966=ADVANCED_FACE('',(#1624),#1010,.T.);
#11017=CLOSED_SHELL('',(#10955,#10956,#10957,#10958,#10959,#10960,#10961,
#10962,#10963,#10964,#10965,#10966));
#12279=AXIS2_PLACEMENT_3D('',#19144,#15260,#15261);
#12280=AXIS2_PLACEMENT_3D('',#19145,#15262,#15263);
#12281=AXIS2_PLACEMENT_3D('',#19154,#15268,#15269);
#12282=AXIS2_PLACEMENT_3D('',#19160,#15273,#15274);
#12283=AXIS2_PLACEMENT_3D('',#19166,#15278,#15279);
#12284=AXIS2_PLACEMENT_3D('',#19172,#15283,#15284);
#12285=AXIS2_PLACEMENT_3D('',#19178,#15288,#15289);
#12286=AXIS2_PLACEMENT_3D('',#19181,#15292,#15293);
#12287=AXIS2_PLACEMENT_3D('',#19182,#15294,#15295);
#12288=AXIS2_PLACEMENT_3D('',#19184,#15296,#15297);
#12289=AXIS2_PLACEMENT_3D('',#19185,#15298,#15299);
#12290=AXIS2_PLACEMENT_3D('',#19187,#15300,#15301);
#12291=AXIS2_PLACEMENT_3D('',#19189,#15303,#15304);
#12292=AXIS2_PLACEMENT_3D('',#19191,#15305,#15306);
#12293=AXIS2_PLACEMENT_3D('',#19193,#15308,#15309);
#12294=AXIS2_PLACEMENT_3D('',#19195,#15310,#15311);
#12295=AXIS2_PLACEMENT_3D('',#19197,#15313,#15314);
#15260=DIRECTION('axis',(0.,0.,1.));
#15261=DIRECTION('refdir',(1.,0.,0.));
#15262=DIRECTION('center_axis',(0.866025403784439,0.,-0.5));
#15263=DIRECTION('ref_axis',(0.5,0.,0.866025403784439));
#15264=DIRECTION('',(0.5,0.,0.866025403784439));
#15265=DIRECTION('',(0.,-1.,0.));
#15266=DIRECTION('',(0.5,0.,0.866025403784439));
#15267=DIRECTION('',(0.,-1.,0.));
#15268=DIRECTION('center_axis',(1.92296268638356E-16,0.,-1.));
#15269=DIRECTION('ref_axis',(1.,0.,1.92296268638356E-16));
#15270=DIRECTION('',(1.,0.,1.92296268638356E-16));
#15271=DIRECTION('',(0.,-1.,0.));
#15272=DIRECTION('',(1.,0.,1.92296268638356E-16));
#15273=DIRECTION('center_axis',(-0.866025403784439,0.,-0.5));
#15274=DIRECTION('ref_axis',(0.5,0.,-0.866025403784439));
#15275=DIRECTION('',(0.5,0.,-0.866025403784439));
#15276=DIRECTION('',(0.,-1.,0.));
#15277=DIRECTION('',(0.5,0.,-0.866025403784438));
#15278=DIRECTION('center_axis',(-0.866025403784439,0.,0.5));
#15279=DIRECTION('ref_axis',(-0.5,0.,-0.866025403784439));
#15280=DIRECTION('',(-0.5,0.,-0.866025403784439));
#15281=DIRECTION('',(0.,-1.,0.));
#15282=DIRECTION('',(-0.5,0.,-0.866025403784439));
#15283=DIRECTION('center_axis',(-1.92296268638356E-16,0.,1.));
#15284=DIRECTION('ref_axis',(-1.,0.,-1.92296268638356E-16));
#15285=DIRECTION('',(-1.,0.,-1.92296268638356E-16));
#15286=DIRECTION('',(0.,-1.,0.));
#15287=DIRECTION('',(-1.,0.,-1.92296268638356E-16));
#15288=DIRECTION('center_axis',(0.866025403784439,0.,0.5));
#15289=DIRECTION('ref_axis',(-0.5,0.,0.866025403784439));
#15290=DIRECTION('',(-0.5,0.,0.866025403784439));
#15291=DIRECTION('',(-0.5,0.,0.866025403784439));
#15292=DIRECTION('center_axis',(0.,-1.,0.));
#15293=DIRECTION('ref_axis',(0.,0.,-1.));
#15294=DIRECTION('center_axis',(0.,1.,0.));
#15295=DIRECTION('ref_axis',(0.,0.,1.));
#15296=DIRECTION('center_axis',(0.,-1.,0.));
#15297=DIRECTION('ref_axis',(1.,0.,0.));
#15298=DIRECTION('center_axis',(0.,-1.,0.));
#15299=DIRECTION('ref_axis',(1.,0.,0.));
#15300=DIRECTION('center_axis',(0.,-1.,0.));
#15301=DIRECTION('ref_axis',(1.,0.,0.));
#15302=DIRECTION('',(0.707106781186547,0.707106781186548,8.65956056235493E-17));
#15303=DIRECTION('center_axis',(0.,-1.,0.));
#15304=DIRECTION('ref_axis',(1.,0.,0.));
#15305=DIRECTION('center_axis',(0.,1.,0.));
#15306=DIRECTION('ref_axis',(1.,0.,0.));
#15307=DIRECTION('',(0.,1.,0.));
#15308=DIRECTION('center_axis',(0.,1.,0.));
#15309=DIRECTION('ref_axis',(1.,0.,0.));
#15310=DIRECTION('center_axis',(0.,-1.,0.));
#15311=DIRECTION('ref_axis',(1.,0.,0.));
#15312=DIRECTION('',(-0.707106781186547,0.707106781186548,-8.65956056235493E-17));
#15313=DIRECTION('center_axis',(0.,-1.,0.));
#15314=DIRECTION('ref_axis',(0.,0.,-1.));
#19144=CARTESIAN_POINT('',(0.,0.,0.));
#19145=CARTESIAN_POINT('Origin',(0.0721687836487032,0.,-0.125));
#19146=CARTESIAN_POINT('',(0.0721687836487032,0.,-0.125));
#19147=CARTESIAN_POINT('',(0.144337567297406,0.,0.));
#19148=CARTESIAN_POINT('',(0.117710979560879,0.,-0.0461186027918559));
#19149=CARTESIAN_POINT('',(0.0721687836487032,-0.25,-0.125));
#19150=CARTESIAN_POINT('',(0.0721687836487032,0.,-0.125));
#19151=CARTESIAN_POINT('',(0.144337567297406,-0.25,0.));
#19152=CARTESIAN_POINT('',(0.144337567297406,-0.25,0.));
#19153=CARTESIAN_POINT('',(0.144337567297406,0.,0.));
#19154=CARTESIAN_POINT('Origin',(-0.0721687836487032,0.,-0.125));
#19155=CARTESIAN_POINT('',(-0.0721687836487032,0.,-0.125));
#19156=CARTESIAN_POINT('',(0.0739156081756484,0.,-0.125));
#19157=CARTESIAN_POINT('',(-0.0721687836487032,-0.25,-0.125));
#19158=CARTESIAN_POINT('',(-0.0721687836487032,0.,-0.125));
#19159=CARTESIAN_POINT('',(0.0721687836487032,-0.25,-0.125));
#19160=CARTESIAN_POINT('Origin',(-0.144337567297406,0.,-4.16333634234434E-17));
#19161=CARTESIAN_POINT('',(-0.144337567297406,0.,-1.76762539787485E-17));
#19162=CARTESIAN_POINT('',(-0.0987953713852306,0.,-0.0788813972081442));
#19163=CARTESIAN_POINT('',(-0.144337567297406,-0.25,-2.77555756156289E-17));
#19164=CARTESIAN_POINT('',(-0.144337567297406,0.,-1.76762539787485E-17));
#19165=CARTESIAN_POINT('',(-0.0721687836487032,-0.25,-0.125));
#19166=CARTESIAN_POINT('Origin',(-0.0721687836487033,0.,0.125));
#19167=CARTESIAN_POINT('',(-0.0721687836487033,0.,0.125));
#19168=CARTESIAN_POINT('',(-0.0627109795608791,0.,0.141381397208144));
#19169=CARTESIAN_POINT('',(-0.0721687836487033,-0.25,0.125));
#19170=CARTESIAN_POINT('',(-0.0721687836487033,0.,0.125));
#19171=CARTESIAN_POINT('',(-0.144337567297406,-0.25,-1.76762539787485E-17));
#19172=CARTESIAN_POINT('Origin',(0.0721687836487032,0.,0.125));
#19173=CARTESIAN_POINT('',(0.0721687836487032,0.,0.125));
#19174=CARTESIAN_POINT('',(0.146084391824352,0.,0.125));
#19175=CARTESIAN_POINT('',(0.0721687836487032,-0.25,0.125));
#19176=CARTESIAN_POINT('',(0.0721687836487032,0.,0.125));
#19177=CARTESIAN_POINT('',(-0.0721687836487033,-0.25,0.125));
#19178=CARTESIAN_POINT('Origin',(0.144337567297406,0.,0.));
#19179=CARTESIAN_POINT('',(0.153795371385231,0.,-0.0163813972081441));
#19180=CARTESIAN_POINT('',(0.0721687836487032,-0.25,0.125));
#19181=CARTESIAN_POINT('Origin',(0.,-0.25,0.));
#19182=CARTESIAN_POINT('Origin',(0.22,0.,0.));
#19183=CARTESIAN_POINT('',(-0.22,-8.67361737988404E-18,-2.69422295812418E-17));
#19184=CARTESIAN_POINT('Origin',(0.,0.,0.));
#19185=CARTESIAN_POINT('Origin',(0.,-0.015,0.));
#19186=CARTESIAN_POINT('',(-0.24505,-0.02505,-3.00099698131059E-17));
#19187=CARTESIAN_POINT('Origin',(0.,-0.02505,0.));
#19188=CARTESIAN_POINT('',(-0.235,-0.015,-2.87791997799628E-17));
#19189=CARTESIAN_POINT('Origin',(0.,-0.3775,0.));
#19190=CARTESIAN_POINT('',(-0.24505,-0.72995,3.00099698131059E-17));
#19191=CARTESIAN_POINT('Origin',(0.,-0.72995,0.));
#19192=CARTESIAN_POINT('',(-0.24505,-0.3775,-3.00099698131059E-17));
#19193=CARTESIAN_POINT('Origin',(0.,-0.7625,0.));
#19194=CARTESIAN_POINT('',(-0.175,-0.8,-2.14313189850787E-17));
#19195=CARTESIAN_POINT('Origin',(0.,-0.8,0.));
#19196=CARTESIAN_POINT('',(-0.2125,-0.7625,-2.60237444818813E-17));
#19197=CARTESIAN_POINT('Origin',(0.,-0.8,0.));
#19321=UNCERTAINTY_MEASURE_WITH_UNIT(LENGTH_MEASURE(0.001),#19362,
'DISTANCE_ACCURACY_VALUE',
'Maximum model space distance between geometric entities at asserted c
onnectivities');
#19323=UNCERTAINTY_MEASURE_WITH_UNIT(LENGTH_MEASURE(0.001),#19362,
'DISTANCE_ACCURACY_VALUE',
'Maximum model space distance between geometric entities at asserted c
onnectivities');
#19359=(
GEOMETRIC_REPRESENTATION_CONTEXT(3)
GLOBAL_UNCERTAINTY_ASSIGNED_CONTEXT((#19321))
GLOBAL_UNIT_ASSIGNED_CONTEXT((#19362,#19364,#19365))
REPRESENTATION_CONTEXT('','3D')
);
#19361=(
GEOMETRIC_REPRESENTATION_CONTEXT(3)
GLOBAL_UNCERTAINTY_ASSIGNED_CONTEXT((#19323))
GLOBAL_UNIT_ASSIGNED_CONTEXT((#19362,#19364,#19365))
REPRESENTATION_CONTEXT('','3D')
);
#19362=(
LENGTH_UNIT()
NAMED_UNIT(*)
SI_UNIT(.CENTI.,.METRE.)
);
#19364=(
NAMED_UNIT(*)
PLANE_ANGLE_UNIT()
SI_UNIT($,.RADIAN.)
);
#19365=(
NAMED_UNIT(*)
SI_UNIT($,.STERADIAN.)
SOLID_ANGLE_UNIT()
);
#19401=SHAPE_DEFINITION_REPRESENTATION(#19468,#19523);
#19468=PRODUCT_DEFINITION_SHAPE('',$,#19561);
#19523=SHAPE_REPRESENTATION('',(#12279),#19359);
#19525=PRODUCT_DEFINITION_CONTEXT('part definition',#19638,'design');
#19561=PRODUCT_DEFINITION('Socket Set Screw - M5x8',
'Socket Set Screw - M5x8',#19598,#19525);
#19598=PRODUCT_DEFINITION_FORMATION('',$,#19675);
#19638=APPLICATION_CONTEXT(
'Core Data for Automotive Mechanical Design Process');
#19639=PRODUCT_CONTEXT('part definition',#19638,'mechanical');
#19675=PRODUCT('Socket Set Screw - M5x8','Socket Set Screw - M5x8',
'Socket Set Screw - M5x8',(#19639));
#19747=COLOUR_RGB('Black',0.12,0.14,0.17);
#19748=FILL_AREA_STYLE_COLOUR('',#19747);
#19749=FILL_AREA_STYLE('',(#19748));
#19750=SURFACE_STYLE_FILL_AREA(#19749);
#19751=SURFACE_SIDE_STYLE('',(#19750));
#19752=SURFACE_STYLE_USAGE(.BOTH.,#19751);
#19753=PRESENTATION_STYLE_ASSIGNMENT((#19752));
ENDSEC;
END-ISO-10303-21;
